ISO-10303-21;
HEADER;
/* Generated by software containing ST-Developer
 * from STEP Tools, Inc. (www.steptools.com) 
 */

FILE_DESCRIPTION(
/* description */ ('Turntable on roller ring'),
/* implementation_level */ '2;1');

FILE_NAME(
/* name */ 'Axle keeper (2).step',
/* time_stamp */ '2026-10-28T03:23:59-07:00',
/* author */ (''),
/* organization */ (''),
/* preprocessor_version */ 'ST-DEVELOPER v20.2',
/* originating_system */ 'Autodesk Translation Framework v15.17.0.0',
/* authorisation */ '');

FILE_SCHEMA (('AUTOMOTIVE_DESIGN { 1 0 10303 214 3 1 1 }'));
ENDSEC;

DATA;
#10=MECHANICAL_DESIGN_GEOMETRIC_PRESENTATION_REPRESENTATION('',(#656),#16281);
#537=SHAPE_REPRESENTATION_RELATIONSHIP('SRR','None',#16556,#592);
#592=ADVANCED_BREP_SHAPE_REPRESENTATION('',(#726),#16250);
#656=STYLED_ITEM('',(#16932),#726);
#726=MANIFOLD_SOLID_BREP('Body1',#8399);
#931=FACE_BOUND('',#2261,.T.);
#932=FACE_BOUND('',#2263,.T.);
#1159=PLANE('',#9761);
#1160=PLANE('',#9762);
#1579=FACE_OUTER_BOUND('',#2258,.T.);
#1580=FACE_OUTER_BOUND('',#2259,.T.);
#1581=FACE_OUTER_BOUND('',#2260,.T.);
#1582=FACE_OUTER_BOUND('',#2262,.T.);
#2258=EDGE_LOOP('',(#7019,#7020,#7021,#7022));
#2259=EDGE_LOOP('',(#7023,#7024,#7025,#7026));
#2260=EDGE_LOOP('',(#7027));
#2261=EDGE_LOOP('',(#7028));
#2262=EDGE_LOOP('',(#7029));
#2263=EDGE_LOOP('',(#7030));
#2837=LINE('',#14984,#3320);
#2838=LINE('',#14990,#3321);
#3320=VECTOR('',#11978,0.225);
#3321=VECTOR('',#11985,0.8);
#3781=CIRCLE('',#9756,0.225);
#3782=CIRCLE('',#9757,0.225);
#3783=CIRCLE('',#9759,0.8);
#3784=CIRCLE('',#9760,0.8);
#4409=VERTEX_POINT('',#14981);
#4410=VERTEX_POINT('',#14983);
#4411=VERTEX_POINT('',#14987);
#4412=VERTEX_POINT('',#14989);
#5320=EDGE_CURVE('',#4409,#4409,#3781,.T.);
#5321=EDGE_CURVE('',#4409,#4410,#2837,.T.);
#5322=EDGE_CURVE('',#4410,#4410,#3782,.T.);
#5323=EDGE_CURVE('',#4411,#4411,#3783,.T.);
#5324=EDGE_CURVE('',#4411,#4412,#2838,.T.);
#5325=EDGE_CURVE('',#4412,#4412,#3784,.T.);
#7019=ORIENTED_EDGE('',*,*,#5320,.F.);
#7020=ORIENTED_EDGE('',*,*,#5321,.T.);
#7021=ORIENTED_EDGE('',*,*,#5322,.T.);
#7022=ORIENTED_EDGE('',*,*,#5321,.F.);
#7023=ORIENTED_EDGE('',*,*,#5323,.F.);
#7024=ORIENTED_EDGE('',*,*,#5324,.T.);
#7025=ORIENTED_EDGE('',*,*,#5325,.T.);
#7026=ORIENTED_EDGE('',*,*,#5324,.F.);
#7027=ORIENTED_EDGE('',*,*,#5323,.T.);
#7028=ORIENTED_EDGE('',*,*,#5320,.T.);
#7029=ORIENTED_EDGE('',*,*,#5325,.F.);
#7030=ORIENTED_EDGE('',*,*,#5322,.F.);
#7796=CYLINDRICAL_SURFACE('',#9755,0.225);
#7797=CYLINDRICAL_SURFACE('',#9758,0.8);
#8182=ADVANCED_FACE('',(#1579),#7796,.F.);
#8183=ADVANCED_FACE('',(#1580),#7797,.T.);
#8184=ADVANCED_FACE('',(#1581,#931),#1159,.T.);
#8185=ADVANCED_FACE('',(#1582,#932),#1160,.F.);
#8399=CLOSED_SHELL('',(#8182,#8183,#8184,#8185));
#9754=AXIS2_PLACEMENT_3D('',#14979,#11972,#11973);
#9755=AXIS2_PLACEMENT_3D('',#14980,#11974,#11975);
#9756=AXIS2_PLACEMENT_3D('',#14982,#11976,#11977);
#9757=AXIS2_PLACEMENT_3D('',#14985,#11979,#11980);
#9758=AXIS2_PLACEMENT_3D('',#14986,#11981,#11982);
#9759=AXIS2_PLACEMENT_3D('',#14988,#11983,#11984);
#9760=AXIS2_PLACEMENT_3D('',#14991,#11986,#11987);
#9761=AXIS2_PLACEMENT_3D('',#14992,#11988,#11989);
#9762=AXIS2_PLACEMENT_3D('',#14993,#11990,#11991);
#11972=DIRECTION('axis',(0.,0.,1.));
#11973=DIRECTION('refdir',(1.,0.,0.));
#11974=DIRECTION('center_axis',(0.,1.,0.));
#11975=DIRECTION('ref_axis',(1.,0.,0.));
#11976=DIRECTION('center_axis',(0.,-1.,0.));
#11977=DIRECTION('ref_axis',(1.,0.,0.));
#11978=DIRECTION('',(0.,-1.,0.));
#11979=DIRECTION('center_axis',(0.,-1.,0.));
#11980=DIRECTION('ref_axis',(1.,0.,0.));
#11981=DIRECTION('center_axis',(0.,1.,0.));
#11982=DIRECTION('ref_axis',(1.,0.,0.));
#11983=DIRECTION('center_axis',(0.,1.,0.));
#11984=DIRECTION('ref_axis',(1.,0.,0.));
#11985=DIRECTION('',(0.,-1.,0.));
#11986=DIRECTION('center_axis',(0.,1.,0.));
#11987=DIRECTION('ref_axis',(1.,0.,0.));
#11988=DIRECTION('center_axis',(0.,1.,0.));
#11989=DIRECTION('ref_axis',(1.,0.,0.));
#11990=DIRECTION('center_axis',(0.,1.,0.));
#11991=DIRECTION('ref_axis',(1.,0.,0.));
#14979=CARTESIAN_POINT('',(0.,0.,0.));
#14980=CARTESIAN_POINT('Origin',(0.,16.3,3.5));
#14981=CARTESIAN_POINT('',(-0.225,16.5,3.5));
#14982=CARTESIAN_POINT('Origin',(0.,16.5,3.5));
#14983=CARTESIAN_POINT('',(-0.225,16.3,3.5));
#14984=CARTESIAN_POINT('',(-0.225,16.3,3.5));
#14985=CARTESIAN_POINT('Origin',(0.,16.3,3.5));
#14986=CARTESIAN_POINT('Origin',(0.,16.3,3.5));
#14987=CARTESIAN_POINT('',(-0.8,16.5,3.5));
#14988=CARTESIAN_POINT('Origin',(0.,16.5,3.5));
#14989=CARTESIAN_POINT('',(-0.8,16.3,3.5));
#14990=CARTESIAN_POINT('',(-0.8,16.3,3.5));
#14991=CARTESIAN_POINT('Origin',(0.,16.3,3.5));
#14992=CARTESIAN_POINT('Origin',(0.,16.5,3.5));
#14993=CARTESIAN_POINT('Origin',(0.,16.3,3.5));
#16181=UNCERTAINTY_MEASURE_WITH_UNIT(LENGTH_MEASURE(0.001),#16282,
'DISTANCE_ACCURACY_VALUE',
'Maximum model space distance between geometric entities at asserted c
onnectivities');
#16212=UNCERTAINTY_MEASURE_WITH_UNIT(LENGTH_MEASURE(0.001),#16282,
'DISTANCE_ACCURACY_VALUE',
'Maximum model space distance between geometric entities at asserted c
onnectivities');
#16250=(
GEOMETRIC_REPRESENTATION_CONTEXT(3)
GLOBAL_UNCERTAINTY_ASSIGNED_CONTEXT((#16181))
GLOBAL_UNIT_ASSIGNED_CONTEXT((#16282,#16284,#16285))
REPRESENTATION_CONTEXT('','3D')
);
#16281=(
GEOMETRIC_REPRESENTATION_CONTEXT(3)
GLOBAL_UNCERTAINTY_ASSIGNED_CONTEXT((#16212))
GLOBAL_UNIT_ASSIGNED_CONTEXT((#16282,#16284,#16285))
REPRESENTATION_CONTEXT('','3D')
);
#16282=(
LENGTH_UNIT()
NAMED_UNIT(*)
SI_UNIT(.CENTI.,.METRE.)
);
#16284=(
NAMED_UNIT(*)
PLANE_ANGLE_UNIT()
SI_UNIT($,.RADIAN.)
);
#16285=(
NAMED_UNIT(*)
SI_UNIT($,.STERADIAN.)
SOLID_ANGLE_UNIT()
);
#16323=SHAPE_DEFINITION_REPRESENTATION(#16417,#16556);
#16417=PRODUCT_DEFINITION_SHAPE('',$,#16625);
#16556=SHAPE_REPRESENTATION('',(#9754),#16250);
#16587=PRODUCT_DEFINITION_CONTEXT('part definition',#16793,'design');
#16625=PRODUCT_DEFINITION('Axle keeper (2)','Axle keeper (2)',#16693,#16587);
#16693=PRODUCT_DEFINITION_FORMATION('',$,#16832);
#16793=APPLICATION_CONTEXT(
'Core Data for Automotive Mechanical Design Process');
#16794=PRODUCT_CONTEXT('part definition',#16793,'mechanical');
#16832=PRODUCT('Axle keeper (2)','Axle keeper (2)','Axle keeper (2)',(#16794));
#16926=COLOUR_RGB('Grey',0.48,0.52,0.57);
#16927=FILL_AREA_STYLE_COLOUR('',#16926);
#16928=FILL_AREA_STYLE('',(#16927));
#16929=SURFACE_STYLE_FILL_AREA(#16928);
#16930=SURFACE_SIDE_STYLE('',(#16929));
#16931=SURFACE_STYLE_USAGE(.BOTH.,#16930);
#16932=PRESENTATION_STYLE_ASSIGNMENT((#16931));
ENDSEC;
END-ISO-10303-21;
